ISO-10303-21;
HEADER;
/* Generated by software containing ST-Developer
 * from STEP Tools, Inc. (www.steptools.com) 
 */

FILE_DESCRIPTION(
/* description */ ('Spring compression tester'),
/* implementation_level */ '2;1');

FILE_NAME(
/* name */ 'Cap Screw - M6x25.step',
/* time_stamp */ '2026-10-28T03:24:11-07:00',
/* author */ (''),
/* organization */ (''),
/* preprocessor_version */ 'ST-DEVELOPER v20.2',
/* originating_system */ 'Autodesk Translation Framework v15.17.0.0',
/* authorisation */ '');

FILE_SCHEMA (('AUTOMOTIVE_DESIGN { 1 0 10303 214 3 1 1 }'));
ENDSEC;

DATA;
#10=MECHANICAL_DESIGN_GEOMETRIC_PRESENTATION_REPRESENTATION('',(#1178),#43521);
#937=ORIENTED_CLOSED_SHELL('',*,#18622,.F.);
#944=BREP_WITH_VOIDS('Body1',#18621,(#937));
#980=CONICAL_SURFACE('',#21159,0.475,0.785398163397449);
#981=CONICAL_SURFACE('',#21163,0.485,0.785398163397448);
#982=CONICAL_SURFACE('',#21167,0.31,0.463647609000806);
#983=CONICAL_SURFACE('',#21171,0.27,0.785398163397448);
#1043=SHAPE_REPRESENTATION_RELATIONSHIP('SRR','None',#43860,#1103);
#1103=ADVANCED_BREP_SHAPE_REPRESENTATION('',(#944),#43520);
#1178=STYLED_ITEM('',(#44209),#944);
#1588=FACE_BOUND('',#4593,.T.);
#2159=PLANE('',#21157);
#2160=PLANE('',#21165);
#2161=PLANE('',#21173);
#2162=PLANE('',#21174);
#2163=PLANE('',#21175);
#2164=PLANE('',#21176);
#2165=PLANE('',#21177);
#2166=PLANE('',#21178);
#2167=PLANE('',#21179);
#2168=PLANE('',#21180);
#2169=PLANE('',#21181);
#3200=FACE_OUTER_BOUND('',#4588,.T.);
#3201=FACE_OUTER_BOUND('',#4589,.T.);
#3202=FACE_OUTER_BOUND('',#4590,.T.);
#3203=FACE_OUTER_BOUND('',#4591,.T.);
#3204=FACE_OUTER_BOUND('',#4592,.T.);
#3205=FACE_OUTER_BOUND('',#4594,.T.);
#3206=FACE_OUTER_BOUND('',#4595,.T.);
#3207=FACE_OUTER_BOUND('',#4596,.T.);
#3208=FACE_OUTER_BOUND('',#4597,.T.);
#3209=FACE_OUTER_BOUND('',#4598,.T.);
#3210=FACE_OUTER_BOUND('',#4599,.T.);
#3211=FACE_OUTER_BOUND('',#4600,.T.);
#3212=FACE_OUTER_BOUND('',#4601,.T.);
#3213=FACE_OUTER_BOUND('',#4602,.T.);
#3214=FACE_OUTER_BOUND('',#4603,.T.);
#3215=FACE_OUTER_BOUND('',#4604,.T.);
#3216=FACE_OUTER_BOUND('',#4605,.T.);
#4588=EDGE_LOOP('',(#17041));
#4589=EDGE_LOOP('',(#17042,#17043,#17044,#17045));
#4590=EDGE_LOOP('',(#17046,#17047,#17048,#17049));
#4591=EDGE_LOOP('',(#17050,#17051,#17052,#17053));
#4592=EDGE_LOOP('',(#17054));
#4593=EDGE_LOOP('',(#17055));
#4594=EDGE_LOOP('',(#17056,#17057,#17058,#17059));
#4595=EDGE_LOOP('',(#17060,#17061,#17062,#17063));
#4596=EDGE_LOOP('',(#17064,#17065,#17066,#17067));
#4597=EDGE_LOOP('',(#17068));
#4598=EDGE_LOOP('',(#17069,#17070,#17071,#17072));
#4599=EDGE_LOOP('',(#17073,#17074,#17075,#17076));
#4600=EDGE_LOOP('',(#17077,#17078,#17079,#17080));
#4601=EDGE_LOOP('',(#17081,#17082,#17083,#17084));
#4602=EDGE_LOOP('',(#17085,#17086,#17087,#17088));
#4603=EDGE_LOOP('',(#17089,#17090,#17091,#17092));
#4604=EDGE_LOOP('',(#17093,#17094,#17095,#17096,#17097,#17098));
#4605=EDGE_LOOP('',(#17099,#17100,#17101,#17102,#17103,#17104));
#6014=LINE('',#43309,#7446);
#6015=LINE('',#43313,#7447);
#6016=LINE('',#43317,#7448);
#6017=LINE('',#43324,#7449);
#6018=LINE('',#43328,#7450);
#6019=LINE('',#43332,#7451);
#6020=LINE('',#43337,#7452);
#6021=LINE('',#43339,#7453);
#6022=LINE('',#43341,#7454);
#6023=LINE('',#43342,#7455);
#6024=LINE('',#43345,#7456);
#6025=LINE('',#43347,#7457);
#6026=LINE('',#43348,#7458);
#6027=LINE('',#43351,#7459);
#6028=LINE('',#43353,#7460);
#6029=LINE('',#43354,#7461);
#6030=LINE('',#43357,#7462);
#6031=LINE('',#43359,#7463);
#6032=LINE('',#43360,#7464);
#6033=LINE('',#43363,#7465);
#6034=LINE('',#43365,#7466);
#6035=LINE('',#43366,#7467);
#6036=LINE('',#43368,#7468);
#6037=LINE('',#43369,#7469);
#7446=VECTOR('',#26358,0.475);
#7447=VECTOR('',#26363,0.5);
#7448=VECTOR('',#26368,0.485);
#7449=VECTOR('',#26377,0.31);
#7450=VECTOR('',#26382,0.3);
#7451=VECTOR('',#26387,0.27);
#7452=VECTOR('',#26392,1.);
#7453=VECTOR('',#26393,1.);
#7454=VECTOR('',#26394,1.);
#7455=VECTOR('',#26395,1.);
#7456=VECTOR('',#26398,1.);
#7457=VECTOR('',#26399,1.);
#7458=VECTOR('',#26400,1.);
#7459=VECTOR('',#26403,1.);
#7460=VECTOR('',#26404,1.);
#7461=VECTOR('',#26405,1.);
#7462=VECTOR('',#26408,1.);
#7463=VECTOR('',#26409,1.);
#7464=VECTOR('',#26410,1.);
#7465=VECTOR('',#26413,1.);
#7466=VECTOR('',#26414,1.);
#7467=VECTOR('',#26415,1.);
#7468=VECTOR('',#26418,1.);
#7469=VECTOR('',#26419,1.);
#8128=CIRCLE('',#21158,0.45);
#8129=CIRCLE('',#21160,0.5);
#8130=CIRCLE('',#21162,0.5);
#8131=CIRCLE('',#21164,0.47);
#8132=CIRCLE('',#21166,0.32);
#8133=CIRCLE('',#21168,0.2942);
#8134=CIRCLE('',#21170,0.2942);
#8135=CIRCLE('',#21172,0.24);
#9753=VERTEX_POINT('',#43304);
#9754=VERTEX_POINT('',#43307);
#9755=VERTEX_POINT('',#43311);
#9756=VERTEX_POINT('',#43315);
#9757=VERTEX_POINT('',#43319);
#9758=VERTEX_POINT('',#43322);
#9759=VERTEX_POINT('',#43326);
#9760=VERTEX_POINT('',#43330);
#9761=VERTEX_POINT('',#43335);
#9762=VERTEX_POINT('',#43336);
#9763=VERTEX_POINT('',#43338);
#9764=VERTEX_POINT('',#43340);
#9765=VERTEX_POINT('',#43344);
#9766=VERTEX_POINT('',#43346);
#9767=VERTEX_POINT('',#43350);
#9768=VERTEX_POINT('',#43352);
#9769=VERTEX_POINT('',#43356);
#9770=VERTEX_POINT('',#43358);
#9771=VERTEX_POINT('',#43362);
#9772=VERTEX_POINT('',#43364);
#12185=EDGE_CURVE('',#9753,#9753,#8128,.T.);
#12186=EDGE_CURVE('',#9754,#9754,#8129,.T.);
#12187=EDGE_CURVE('',#9754,#9753,#6014,.T.);
#12188=EDGE_CURVE('',#9755,#9755,#8130,.T.);
#12189=EDGE_CURVE('',#9755,#9754,#6015,.T.);
#12190=EDGE_CURVE('',#9756,#9756,#8131,.T.);
#12191=EDGE_CURVE('',#9756,#9755,#6016,.T.);
#12192=EDGE_CURVE('',#9757,#9757,#8132,.T.);
#12193=EDGE_CURVE('',#9758,#9758,#8133,.F.);
#12194=EDGE_CURVE('',#9758,#9757,#6017,.T.);
#12195=EDGE_CURVE('',#9759,#9759,#8134,.F.);
#12196=EDGE_CURVE('',#9759,#9758,#6018,.T.);
#12197=EDGE_CURVE('',#9760,#9760,#8135,.T.);
#12198=EDGE_CURVE('',#9760,#9759,#6019,.T.);
#12199=EDGE_CURVE('',#9761,#9762,#6020,.T.);
#12200=EDGE_CURVE('',#9762,#9763,#6021,.T.);
#12201=EDGE_CURVE('',#9763,#9764,#6022,.T.);
#12202=EDGE_CURVE('',#9761,#9764,#6023,.T.);
#12203=EDGE_CURVE('',#9762,#9765,#6024,.T.);
#12204=EDGE_CURVE('',#9765,#9766,#6025,.T.);
#12205=EDGE_CURVE('',#9766,#9763,#6026,.T.);
#12206=EDGE_CURVE('',#9765,#9767,#6027,.T.);
#12207=EDGE_CURVE('',#9767,#9768,#6028,.T.);
#12208=EDGE_CURVE('',#9768,#9766,#6029,.T.);
#12209=EDGE_CURVE('',#9767,#9769,#6030,.T.);
#12210=EDGE_CURVE('',#9769,#9770,#6031,.T.);
#12211=EDGE_CURVE('',#9770,#9768,#6032,.T.);
#12212=EDGE_CURVE('',#9769,#9771,#6033,.T.);
#12213=EDGE_CURVE('',#9771,#9772,#6034,.T.);
#12214=EDGE_CURVE('',#9772,#9770,#6035,.T.);
#12215=EDGE_CURVE('',#9771,#9761,#6036,.T.);
#12216=EDGE_CURVE('',#9764,#9772,#6037,.T.);
#17041=ORIENTED_EDGE('',*,*,#12185,.F.);
#17042=ORIENTED_EDGE('',*,*,#12186,.F.);
#17043=ORIENTED_EDGE('',*,*,#12187,.T.);
#17044=ORIENTED_EDGE('',*,*,#12185,.T.);
#17045=ORIENTED_EDGE('',*,*,#12187,.F.);
#17046=ORIENTED_EDGE('',*,*,#12188,.F.);
#17047=ORIENTED_EDGE('',*,*,#12189,.T.);
#17048=ORIENTED_EDGE('',*,*,#12186,.T.);
#17049=ORIENTED_EDGE('',*,*,#12189,.F.);
#17050=ORIENTED_EDGE('',*,*,#12190,.F.);
#17051=ORIENTED_EDGE('',*,*,#12191,.T.);
#17052=ORIENTED_EDGE('',*,*,#12188,.T.);
#17053=ORIENTED_EDGE('',*,*,#12191,.F.);
#17054=ORIENTED_EDGE('',*,*,#12190,.T.);
#17055=ORIENTED_EDGE('',*,*,#12192,.F.);
#17056=ORIENTED_EDGE('',*,*,#12193,.F.);
#17057=ORIENTED_EDGE('',*,*,#12194,.T.);
#17058=ORIENTED_EDGE('',*,*,#12192,.T.);
#17059=ORIENTED_EDGE('',*,*,#12194,.F.);
#17060=ORIENTED_EDGE('',*,*,#12195,.F.);
#17061=ORIENTED_EDGE('',*,*,#12196,.T.);
#17062=ORIENTED_EDGE('',*,*,#12193,.T.);
#17063=ORIENTED_EDGE('',*,*,#12196,.F.);
#17064=ORIENTED_EDGE('',*,*,#12197,.F.);
#17065=ORIENTED_EDGE('',*,*,#12198,.T.);
#17066=ORIENTED_EDGE('',*,*,#12195,.T.);
#17067=ORIENTED_EDGE('',*,*,#12198,.F.);
#17068=ORIENTED_EDGE('',*,*,#12197,.T.);
#17069=ORIENTED_EDGE('',*,*,#12199,.T.);
#17070=ORIENTED_EDGE('',*,*,#12200,.T.);
#17071=ORIENTED_EDGE('',*,*,#12201,.T.);
#17072=ORIENTED_EDGE('',*,*,#12202,.F.);
#17073=ORIENTED_EDGE('',*,*,#12203,.T.);
#17074=ORIENTED_EDGE('',*,*,#12204,.T.);
#17075=ORIENTED_EDGE('',*,*,#12205,.T.);
#17076=ORIENTED_EDGE('',*,*,#12200,.F.);
#17077=ORIENTED_EDGE('',*,*,#12206,.T.);
#17078=ORIENTED_EDGE('',*,*,#12207,.T.);
#17079=ORIENTED_EDGE('',*,*,#12208,.T.);
#17080=ORIENTED_EDGE('',*,*,#12204,.F.);
#17081=ORIENTED_EDGE('',*,*,#12209,.T.);
#17082=ORIENTED_EDGE('',*,*,#12210,.T.);
#17083=ORIENTED_EDGE('',*,*,#12211,.T.);
#17084=ORIENTED_EDGE('',*,*,#12207,.F.);
#17085=ORIENTED_EDGE('',*,*,#12212,.T.);
#17086=ORIENTED_EDGE('',*,*,#12213,.T.);
#17087=ORIENTED_EDGE('',*,*,#12214,.T.);
#17088=ORIENTED_EDGE('',*,*,#12210,.F.);
#17089=ORIENTED_EDGE('',*,*,#12215,.T.);
#17090=ORIENTED_EDGE('',*,*,#12202,.T.);
#17091=ORIENTED_EDGE('',*,*,#12216,.T.);
#17092=ORIENTED_EDGE('',*,*,#12213,.F.);
#17093=ORIENTED_EDGE('',*,*,#12215,.F.);
#17094=ORIENTED_EDGE('',*,*,#12212,.F.);
#17095=ORIENTED_EDGE('',*,*,#12209,.F.);
#17096=ORIENTED_EDGE('',*,*,#12206,.F.);
#17097=ORIENTED_EDGE('',*,*,#12203,.F.);
#17098=ORIENTED_EDGE('',*,*,#12199,.F.);
#17099=ORIENTED_EDGE('',*,*,#12216,.F.);
#17100=ORIENTED_EDGE('',*,*,#12201,.F.);
#17101=ORIENTED_EDGE('',*,*,#12205,.F.);
#17102=ORIENTED_EDGE('',*,*,#12208,.F.);
#17103=ORIENTED_EDGE('',*,*,#12211,.F.);
#17104=ORIENTED_EDGE('',*,*,#12214,.F.);
#17492=CYLINDRICAL_SURFACE('',#21161,0.5);
#17493=CYLINDRICAL_SURFACE('',#21169,0.2942);
#18524=ADVANCED_FACE('',(#3200),#2159,.T.);
#18525=ADVANCED_FACE('',(#3201),#980,.T.);
#18526=ADVANCED_FACE('',(#3202),#17492,.T.);
#18527=ADVANCED_FACE('',(#3203),#981,.T.);
#18528=ADVANCED_FACE('',(#3204,#1588),#2160,.T.);
#18529=ADVANCED_FACE('',(#3205),#982,.T.);
#18530=ADVANCED_FACE('',(#3206),#17493,.T.);
#18531=ADVANCED_FACE('',(#3207),#983,.T.);
#18532=ADVANCED_FACE('',(#3208),#2161,.T.);
#18533=ADVANCED_FACE('',(#3209),#2162,.F.);
#18534=ADVANCED_FACE('',(#3210),#2163,.F.);
#18535=ADVANCED_FACE('',(#3211),#2164,.F.);
#18536=ADVANCED_FACE('',(#3212),#2165,.F.);
#18537=ADVANCED_FACE('',(#3213),#2166,.F.);
#18538=ADVANCED_FACE('',(#3214),#2167,.F.);
#18539=ADVANCED_FACE('',(#3215),#2168,.F.);
#18540=ADVANCED_FACE('',(#3216),#2169,.F.);
#18621=CLOSED_SHELL('',(#18524,#18525,#18526,#18527,#18528,#18529,#18530,
#18531,#18532));
#18622=CLOSED_SHELL('',(#18533,#18534,#18535,#18536,#18537,#18538,#18539,
#18540));
#21156=AXIS2_PLACEMENT_3D('',#43302,#26348,#26349);
#21157=AXIS2_PLACEMENT_3D('',#43303,#26350,#26351);
#21158=AXIS2_PLACEMENT_3D('',#43305,#26352,#26353);
#21159=AXIS2_PLACEMENT_3D('',#43306,#26354,#26355);
#21160=AXIS2_PLACEMENT_3D('',#43308,#26356,#26357);
#21161=AXIS2_PLACEMENT_3D('',#43310,#26359,#26360);
#21162=AXIS2_PLACEMENT_3D('',#43312,#26361,#26362);
#21163=AXIS2_PLACEMENT_3D('',#43314,#26364,#26365);
#21164=AXIS2_PLACEMENT_3D('',#43316,#26366,#26367);
#21165=AXIS2_PLACEMENT_3D('',#43318,#26369,#26370);
#21166=AXIS2_PLACEMENT_3D('',#43320,#26371,#26372);
#21167=AXIS2_PLACEMENT_3D('',#43321,#26373,#26374);
#21168=AXIS2_PLACEMENT_3D('',#43323,#26375,#26376);
#21169=AXIS2_PLACEMENT_3D('',#43325,#26378,#26379);
#21170=AXIS2_PLACEMENT_3D('',#43327,#26380,#26381);
#21171=AXIS2_PLACEMENT_3D('',#43329,#26383,#26384);
#21172=AXIS2_PLACEMENT_3D('',#43331,#26385,#26386);
#21173=AXIS2_PLACEMENT_3D('',#43333,#26388,#26389);
#21174=AXIS2_PLACEMENT_3D('',#43334,#26390,#26391);
#21175=AXIS2_PLACEMENT_3D('',#43343,#26396,#26397);
#21176=AXIS2_PLACEMENT_3D('',#43349,#26401,#26402);
#21177=AXIS2_PLACEMENT_3D('',#43355,#26406,#26407);
#21178=AXIS2_PLACEMENT_3D('',#43361,#26411,#26412);
#21179=AXIS2_PLACEMENT_3D('',#43367,#26416,#26417);
#21180=AXIS2_PLACEMENT_3D('',#43370,#26420,#26421);
#21181=AXIS2_PLACEMENT_3D('',#43371,#26422,#26423);
#26348=DIRECTION('axis',(0.,0.,1.));
#26349=DIRECTION('refdir',(1.,0.,0.));
#26350=DIRECTION('center_axis',(0.,1.,0.));
#26351=DIRECTION('ref_axis',(0.,0.,1.));
#26352=DIRECTION('center_axis',(0.,-1.,0.));
#26353=DIRECTION('ref_axis',(1.,0.,0.));
#26354=DIRECTION('center_axis',(0.,-1.,0.));
#26355=DIRECTION('ref_axis',(1.,0.,0.));
#26356=DIRECTION('center_axis',(0.,-1.,0.));
#26357=DIRECTION('ref_axis',(1.,0.,0.));
#26358=DIRECTION('',(0.707106781186548,0.707106781186547,8.65956056235494E-17));
#26359=DIRECTION('center_axis',(0.,-1.,0.));
#26360=DIRECTION('ref_axis',(1.,0.,0.));
#26361=DIRECTION('center_axis',(0.,-1.,0.));
#26362=DIRECTION('ref_axis',(1.,0.,0.));
#26363=DIRECTION('',(0.,1.,0.));
#26364=DIRECTION('center_axis',(0.,1.,0.));
#26365=DIRECTION('ref_axis',(1.,0.,0.));
#26366=DIRECTION('center_axis',(0.,-1.,0.));
#26367=DIRECTION('ref_axis',(1.,0.,0.));
#26368=DIRECTION('',(-0.707106781186547,0.707106781186548,-8.65956056235493E-17));
#26369=DIRECTION('center_axis',(0.,-1.,0.));
#26370=DIRECTION('ref_axis',(0.,0.,-1.));
#26371=DIRECTION('center_axis',(0.,-1.,0.));
#26372=DIRECTION('ref_axis',(1.,0.,0.));
#26373=DIRECTION('center_axis',(0.,1.,0.));
#26374=DIRECTION('ref_axis',(1.,0.,0.));
#26375=DIRECTION('center_axis',(0.,1.,0.));
#26376=DIRECTION('ref_axis',(1.,0.,0.));
#26377=DIRECTION('',(-0.447213595499958,0.894427190999916,-5.47678698264203E-17));
#26378=DIRECTION('center_axis',(0.,-1.,0.));
#26379=DIRECTION('ref_axis',(1.,0.,0.));
#26380=DIRECTION('center_axis',(0.,1.,0.));
#26381=DIRECTION('ref_axis',(1.,0.,0.));
#26382=DIRECTION('',(0.,1.,0.));
#26383=DIRECTION('center_axis',(0.,1.,0.));
#26384=DIRECTION('ref_axis',(1.,0.,0.));
#26385=DIRECTION('center_axis',(0.,-1.,0.));
#26386=DIRECTION('ref_axis',(1.,0.,0.));
#26387=DIRECTION('',(-0.707106781186547,0.707106781186548,-8.65956056235493E-17));
#26388=DIRECTION('center_axis',(0.,-1.,0.));
#26389=DIRECTION('ref_axis',(0.,0.,-1.));
#26390=DIRECTION('center_axis',(0.866025403784439,0.,-0.5));
#26391=DIRECTION('ref_axis',(0.5,0.,0.866025403784439));
#26392=DIRECTION('',(-0.5,0.,-0.866025403784439));
#26393=DIRECTION('',(0.,-1.,0.));
#26394=DIRECTION('',(0.5,0.,0.866025403784439));
#26395=DIRECTION('',(0.,-1.,0.));
#26396=DIRECTION('center_axis',(1.92296268638356E-16,0.,-1.));
#26397=DIRECTION('ref_axis',(1.,0.,1.92296268638356E-16));
#26398=DIRECTION('',(-1.,0.,-1.92296268638356E-16));
#26399=DIRECTION('',(0.,-1.,0.));
#26400=DIRECTION('',(1.,0.,1.92296268638356E-16));
#26401=DIRECTION('center_axis',(-0.866025403784439,0.,-0.5));
#26402=DIRECTION('ref_axis',(0.5,0.,-0.866025403784439));
#26403=DIRECTION('',(-0.5,0.,0.866025403784438));
#26404=DIRECTION('',(0.,-1.,0.));
#26405=DIRECTION('',(0.5,0.,-0.866025403784438));
#26406=DIRECTION('center_axis',(-0.866025403784439,0.,0.5));
#26407=DIRECTION('ref_axis',(-0.5,0.,-0.866025403784439));
#26408=DIRECTION('',(0.5,0.,0.866025403784439));
#26409=DIRECTION('',(0.,-1.,0.));
#26410=DIRECTION('',(-0.5,0.,-0.866025403784439));
#26411=DIRECTION('center_axis',(-1.92296268638356E-16,0.,1.));
#26412=DIRECTION('ref_axis',(-1.,0.,-1.92296268638356E-16));
#26413=DIRECTION('',(1.,0.,1.92296268638356E-16));
#26414=DIRECTION('',(0.,-1.,0.));
#26415=DIRECTION('',(-1.,0.,-1.92296268638356E-16));
#26416=DIRECTION('center_axis',(0.866025403784439,0.,0.5));
#26417=DIRECTION('ref_axis',(-0.5,0.,0.866025403784439));
#26418=DIRECTION('',(0.5,0.,-0.866025403784439));
#26419=DIRECTION('',(-0.5,0.,0.866025403784439));
#26420=DIRECTION('center_axis',(0.,1.,0.));
#26421=DIRECTION('ref_axis',(1.,0.,0.));
#26422=DIRECTION('center_axis',(0.,-1.,0.));
#26423=DIRECTION('ref_axis',(0.,0.,-1.));
#43302=CARTESIAN_POINT('',(0.,0.,0.));
#43303=CARTESIAN_POINT('Origin',(0.45,0.6,0.));
#43304=CARTESIAN_POINT('',(-0.45,0.6,-5.51091059616309E-17));
#43305=CARTESIAN_POINT('Origin',(0.,0.6,0.));
#43306=CARTESIAN_POINT('Origin',(0.,0.575,0.));
#43307=CARTESIAN_POINT('',(-0.5,0.55,-6.12323399573677E-17));
#43308=CARTESIAN_POINT('Origin',(0.,0.55,0.));
#43309=CARTESIAN_POINT('',(-0.475,0.575,-5.81707229594993E-17));
#43310=CARTESIAN_POINT('Origin',(0.,0.29,0.));
#43311=CARTESIAN_POINT('',(-0.5,0.0299999999999998,-6.12323399573677E-17));
#43312=CARTESIAN_POINT('Origin',(0.,0.0299999999999998,0.));
#43313=CARTESIAN_POINT('',(-0.5,0.29,-6.12323399573677E-17));
#43314=CARTESIAN_POINT('Origin',(0.,0.0150000000000001,0.));
#43315=CARTESIAN_POINT('',(-0.47,7.11236625150491E-17,-5.75583995599256E-17));
#43316=CARTESIAN_POINT('Origin',(0.,0.,0.));
#43317=CARTESIAN_POINT('',(-0.485,0.0150000000000001,-5.93953697586466E-17));
#43318=CARTESIAN_POINT('Origin',(0.32,0.,0.));
#43319=CARTESIAN_POINT('',(-0.32,-6.93889390390723E-18,-3.91886975727153E-17));
#43320=CARTESIAN_POINT('Origin',(0.,0.,0.));
#43321=CARTESIAN_POINT('Origin',(0.,-0.02,0.));
#43322=CARTESIAN_POINT('',(-0.2942,-0.0515999999999999,3.60291088309151E-17));
#43323=CARTESIAN_POINT('Origin',(0.,-0.0515999999999999,0.));
#43324=CARTESIAN_POINT('',(-0.31,-0.02,-3.7964050773568E-17));
#43325=CARTESIAN_POINT('Origin',(0.,-1.24,0.));
#43326=CARTESIAN_POINT('',(-0.2942,-2.4458,3.60291088309151E-17));
#43327=CARTESIAN_POINT('Origin',(0.,-2.4458,0.));
#43328=CARTESIAN_POINT('',(-0.2942,-1.24,-3.60291088309151E-17));
#43329=CARTESIAN_POINT('Origin',(0.,-2.47,0.));
#43330=CARTESIAN_POINT('',(-0.24,-2.5,-2.93915231795365E-17));
#43331=CARTESIAN_POINT('Origin',(0.,-2.5,0.));
#43332=CARTESIAN_POINT('',(-0.27,-2.47,-3.30654635769785E-17));
#43333=CARTESIAN_POINT('Origin',(0.,-2.5,0.));
#43334=CARTESIAN_POINT('Origin',(0.144337567297406,-0.6,-0.25));
#43335=CARTESIAN_POINT('',(0.288675134594813,-0.6,0.));
#43336=CARTESIAN_POINT('',(0.144337567297406,-0.6,-0.25));
#43337=CARTESIAN_POINT('',(0.288675134594813,-0.6,0.));
#43338=CARTESIAN_POINT('',(0.144337567297406,-0.96,-0.25));
#43339=CARTESIAN_POINT('',(0.144337567297406,-0.6,-0.25));
#43340=CARTESIAN_POINT('',(0.288675134594813,-0.96,0.));
#43341=CARTESIAN_POINT('',(0.288675134594813,-0.96,0.));
#43342=CARTESIAN_POINT('',(0.288675134594813,-0.6,0.));
#43343=CARTESIAN_POINT('Origin',(-0.144337567297406,-0.6,-0.25));
#43344=CARTESIAN_POINT('',(-0.144337567297406,-0.6,-0.25));
#43345=CARTESIAN_POINT('',(0.144337567297406,-0.6,-0.25));
#43346=CARTESIAN_POINT('',(-0.144337567297406,-0.96,-0.25));
#43347=CARTESIAN_POINT('',(-0.144337567297406,-0.6,-0.25));
#43348=CARTESIAN_POINT('',(0.144337567297406,-0.96,-0.25));
#43349=CARTESIAN_POINT('Origin',(-0.288675134594813,-0.6,-8.32667268468867E-17));
#43350=CARTESIAN_POINT('',(-0.288675134594813,-0.6,-3.53525079574969E-17));
#43351=CARTESIAN_POINT('',(-0.144337567297406,-0.6,-0.25));
#43352=CARTESIAN_POINT('',(-0.288675134594813,-0.96,-5.55111512312578E-17));
#43353=CARTESIAN_POINT('',(-0.288675134594813,-0.6,-3.53525079574969E-17));
#43354=CARTESIAN_POINT('',(-0.144337567297406,-0.96,-0.25));
#43355=CARTESIAN_POINT('Origin',(-0.144337567297407,-0.6,0.25));
#43356=CARTESIAN_POINT('',(-0.144337567297407,-0.6,0.25));
#43357=CARTESIAN_POINT('',(-0.288675134594813,-0.6,-3.53525079574969E-17));
#43358=CARTESIAN_POINT('',(-0.144337567297407,-0.96,0.25));
#43359=CARTESIAN_POINT('',(-0.144337567297407,-0.6,0.25));
#43360=CARTESIAN_POINT('',(-0.288675134594813,-0.96,-3.53525079574969E-17));
#43361=CARTESIAN_POINT('Origin',(0.144337567297406,-0.6,0.25));
#43362=CARTESIAN_POINT('',(0.144337567297406,-0.6,0.25));
#43363=CARTESIAN_POINT('',(-0.144337567297407,-0.6,0.25));
#43364=CARTESIAN_POINT('',(0.144337567297406,-0.96,0.25));
#43365=CARTESIAN_POINT('',(0.144337567297406,-0.6,0.25));
#43366=CARTESIAN_POINT('',(-0.144337567297407,-0.96,0.25));
#43367=CARTESIAN_POINT('Origin',(0.288675134594813,-0.6,0.));
#43368=CARTESIAN_POINT('',(0.144337567297406,-0.6,0.25));
#43369=CARTESIAN_POINT('',(0.144337567297406,-0.96,0.25));
#43370=CARTESIAN_POINT('Origin',(0.,-0.6,0.));
#43371=CARTESIAN_POINT('Origin',(0.,-0.96,0.));
#43452=UNCERTAINTY_MEASURE_WITH_UNIT(LENGTH_MEASURE(0.001),#43522,
'DISTANCE_ACCURACY_VALUE',
'Maximum model space distance between geometric entities at asserted c
onnectivities');
#43453=UNCERTAINTY_MEASURE_WITH_UNIT(LENGTH_MEASURE(0.001),#43522,
'DISTANCE_ACCURACY_VALUE',
'Maximum model space distance between geometric entities at asserted c
onnectivities');
#43520=(
GEOMETRIC_REPRESENTATION_CONTEXT(3)
GLOBAL_UNCERTAINTY_ASSIGNED_CONTEXT((#43452))
GLOBAL_UNIT_ASSIGNED_CONTEXT((#43522,#43524,#43525))
REPRESENTATION_CONTEXT('','3D')
);
#43521=(
GEOMETRIC_REPRESENTATION_CONTEXT(3)
GLOBAL_UNCERTAINTY_ASSIGNED_CONTEXT((#43453))
GLOBAL_UNIT_ASSIGNED_CONTEXT((#43522,#43524,#43525))
REPRESENTATION_CONTEXT('','3D')
);
#43522=(
LENGTH_UNIT()
NAMED_UNIT(*)
SI_UNIT(.CENTI.,.METRE.)
);
#43524=(
NAMED_UNIT(*)
PLANE_ANGLE_UNIT()
SI_UNIT($,.RADIAN.)
);
#43525=(
NAMED_UNIT(*)
SI_UNIT($,.STERADIAN.)
SOLID_ANGLE_UNIT()
);
#43592=SHAPE_DEFINITION_REPRESENTATION(#43779,#43860);
#43779=PRODUCT_DEFINITION_SHAPE('',$,#43928);
#43860=SHAPE_REPRESENTATION('',(#21156),#43520);
#43861=PRODUCT_DEFINITION_CONTEXT('part definition',#44064,'design');
#43928=PRODUCT_DEFINITION('Cap Screw - M6x25','Cap Screw - M6x25',#43995,
#43861);
#43995=PRODUCT_DEFINITION_FORMATION('',$,#44132);
#44064=APPLICATION_CONTEXT(
'Core Data for Automotive Mechanical Design Process');
#44065=PRODUCT_CONTEXT('part definition',#44064,'mechanical');
#44132=PRODUCT('Cap Screw - M6x25','Cap Screw - M6x25',
'Cap Screw - M6x25',(#44065));
#44203=COLOUR_RGB('Black',0.12,0.14,0.17);
#44204=FILL_AREA_STYLE_COLOUR('',#44203);
#44205=FILL_AREA_STYLE('',(#44204));
#44206=SURFACE_STYLE_FILL_AREA(#44205);
#44207=SURFACE_SIDE_STYLE('',(#44206));
#44208=SURFACE_STYLE_USAGE(.BOTH.,#44207);
#44209=PRESENTATION_STYLE_ASSIGNMENT((#44208));
ENDSEC;
END-ISO-10303-21;
